ISO-10303-21;
HEADER;
/* Generated by software containing ST-Developer
 * from STEP Tools, Inc. (www.steptools.com) 
 */

FILE_DESCRIPTION(
/* description */ ('PAT-091'),
/* implementation_level */ '2;1');

FILE_NAME(
/* name */ 'M4 low-profile retaining screw (2).step',
/* time_stamp */ '2026-10-27T15:34:44-07:00',
/* author */ (''),
/* organization */ (''),
/* preprocessor_version */ 'ST-DEVELOPER v20.2',
/* originating_system */ 'Autodesk Translation Framework v15.17.0.0',
/* authorisation */ '');

FILE_SCHEMA (('AUTOMOTIVE_DESIGN { 1 0 10303 214 3 1 1 }'));
ENDSEC;

DATA;
#10=MECHANICAL_DESIGN_GEOMETRIC_PRESENTATION_REPRESENTATION('',(#1050),#25100);
#830=SHAPE_REPRESENTATION_RELATIONSHIP('SRR','None',#25597,#940);
#940=ADVANCED_BREP_SHAPE_REPRESENTATION('',(#1171),#25067);
#1050=STYLED_ITEM('',(#26198),#1171);
#1171=MANIFOLD_SOLID_BREP('Body1',#13330);
#1555=FACE_BOUND('',#3815,.T.);
#1966=PLANE('',#15872);
#1967=PLANE('',#15877);
#1968=PLANE('',#15880);
#2656=FACE_OUTER_BOUND('',#3814,.T.);
#2657=FACE_OUTER_BOUND('',#3816,.T.);
#2658=FACE_OUTER_BOUND('',#3817,.T.);
#2659=FACE_OUTER_BOUND('',#3818,.T.);
#2660=FACE_OUTER_BOUND('',#3819,.T.);
#3814=EDGE_LOOP('',(#11318));
#3815=EDGE_LOOP('',(#11319));
#3816=EDGE_LOOP('',(#11320,#11321,#11322,#11323));
#3817=EDGE_LOOP('',(#11324));
#3818=EDGE_LOOP('',(#11325,#11326,#11327,#11328));
#3819=EDGE_LOOP('',(#11329));
#4761=LINE('',#23739,#5501);
#4762=LINE('',#23745,#5502);
#5501=VECTOR('',#19687,0.350000000000001);
#5502=VECTOR('',#19696,0.199999999999999);
#6136=CIRCLE('',#15873,0.350000000000001);
#6137=CIRCLE('',#15874,0.199999999999999);
#6138=CIRCLE('',#15876,0.350000000000001);
#6139=CIRCLE('',#15879,0.199999999999999);
#7161=VERTEX_POINT('',#23733);
#7162=VERTEX_POINT('',#23735);
#7163=VERTEX_POINT('',#23738);
#7164=VERTEX_POINT('',#23743);
#8594=EDGE_CURVE('',#7161,#7161,#6136,.T.);
#8595=EDGE_CURVE('',#7162,#7162,#6137,.T.);
#8596=EDGE_CURVE('',#7161,#7163,#4761,.T.);
#8597=EDGE_CURVE('',#7163,#7163,#6138,.T.);
#8598=EDGE_CURVE('',#7164,#7164,#6139,.T.);
#8599=EDGE_CURVE('',#7164,#7162,#4762,.T.);
#11318=ORIENTED_EDGE('',*,*,#8594,.T.);
#11319=ORIENTED_EDGE('',*,*,#8595,.F.);
#11320=ORIENTED_EDGE('',*,*,#8594,.F.);
#11321=ORIENTED_EDGE('',*,*,#8596,.T.);
#11322=ORIENTED_EDGE('',*,*,#8597,.T.);
#11323=ORIENTED_EDGE('',*,*,#8596,.F.);
#11324=ORIENTED_EDGE('',*,*,#8597,.F.);
#11325=ORIENTED_EDGE('',*,*,#8598,.F.);
#11326=ORIENTED_EDGE('',*,*,#8599,.T.);
#11327=ORIENTED_EDGE('',*,*,#8595,.T.);
#11328=ORIENTED_EDGE('',*,*,#8599,.F.);
#11329=ORIENTED_EDGE('',*,*,#8598,.T.);
#12329=CYLINDRICAL_SURFACE('',#15875,0.350000000000001);
#12330=CYLINDRICAL_SURFACE('',#15878,0.199999999999999);
#13023=ADVANCED_FACE('',(#2656,#1555),#1966,.T.);
#13024=ADVANCED_FACE('',(#2657),#12329,.T.);
#13025=ADVANCED_FACE('',(#2658),#1967,.F.);
#13026=ADVANCED_FACE('',(#2659),#12330,.T.);
#13027=ADVANCED_FACE('',(#2660),#1968,.T.);
#13330=CLOSED_SHELL('',(#13023,#13024,#13025,#13026,#13027));
#15871=AXIS2_PLACEMENT_3D('',#23731,#19677,#19678);
#15872=AXIS2_PLACEMENT_3D('',#23732,#19679,#19680);
#15873=AXIS2_PLACEMENT_3D('',#23734,#19681,#19682);
#15874=AXIS2_PLACEMENT_3D('',#23736,#19683,#19684);
#15875=AXIS2_PLACEMENT_3D('',#23737,#19685,#19686);
#15876=AXIS2_PLACEMENT_3D('',#23740,#19688,#19689);
#15877=AXIS2_PLACEMENT_3D('',#23741,#19690,#19691);
#15878=AXIS2_PLACEMENT_3D('',#23742,#19692,#19693);
#15879=AXIS2_PLACEMENT_3D('',#23744,#19694,#19695);
#15880=AXIS2_PLACEMENT_3D('',#23746,#19697,#19698);
#19677=DIRECTION('axis',(0.,0.,1.));
#19678=DIRECTION('refdir',(1.,0.,0.));
#19679=DIRECTION('center_axis',(0.,1.,0.));
#19680=DIRECTION('ref_axis',(1.,0.,0.));
#19681=DIRECTION('center_axis',(0.,1.,0.));
#19682=DIRECTION('ref_axis',(1.,0.,0.));
#19683=DIRECTION('center_axis',(0.,1.,0.));
#19684=DIRECTION('ref_axis',(1.,0.,0.));
#19685=DIRECTION('center_axis',(0.,1.,0.));
#19686=DIRECTION('ref_axis',(1.,0.,0.));
#19687=DIRECTION('',(0.,-1.,0.));
#19688=DIRECTION('center_axis',(0.,1.,0.));
#19689=DIRECTION('ref_axis',(1.,0.,0.));
#19690=DIRECTION('center_axis',(0.,1.,0.));
#19691=DIRECTION('ref_axis',(1.,0.,0.));
#19692=DIRECTION('center_axis',(0.,1.,0.));
#19693=DIRECTION('ref_axis',(1.,0.,0.));
#19694=DIRECTION('center_axis',(0.,1.,0.));
#19695=DIRECTION('ref_axis',(1.,0.,0.));
#19696=DIRECTION('',(0.,-1.,0.));
#19697=DIRECTION('center_axis',(0.,1.,0.));
#19698=DIRECTION('ref_axis',(1.,0.,0.));
#23731=CARTESIAN_POINT('',(0.,0.,0.));
#23732=CARTESIAN_POINT('Origin',(18.056769185842,-5.8,6.69185245480489));
#23733=CARTESIAN_POINT('',(17.706769185842,-5.8,6.69185245480489));
#23734=CARTESIAN_POINT('Origin',(18.056769185842,-5.8,6.69185245480489));
#23735=CARTESIAN_POINT('',(17.856769185842,-5.8,6.69185245480489));
#23736=CARTESIAN_POINT('Origin',(18.056769185842,-5.8,6.69185245480489));
#23737=CARTESIAN_POINT('Origin',(18.056769185842,-5.9,6.69185245480489));
#23738=CARTESIAN_POINT('',(17.706769185842,-5.9,6.69185245480489));
#23739=CARTESIAN_POINT('',(17.706769185842,-5.9,6.69185245480489));
#23740=CARTESIAN_POINT('Origin',(18.056769185842,-5.9,6.69185245480489));
#23741=CARTESIAN_POINT('Origin',(18.056769185842,-5.9,6.69185245480489));
#23742=CARTESIAN_POINT('Origin',(18.056769185842,-5.8,6.69185245480489));
#23743=CARTESIAN_POINT('',(17.856769185842,-5.1,6.69185245480489));
#23744=CARTESIAN_POINT('Origin',(18.056769185842,-5.1,6.69185245480489));
#23745=CARTESIAN_POINT('',(17.856769185842,-5.8,6.69185245480489));
#23746=CARTESIAN_POINT('Origin',(18.056769185842,-5.1,6.69185245480489));
#24946=UNCERTAINTY_MEASURE_WITH_UNIT(LENGTH_MEASURE(0.001),#25101,
'DISTANCE_ACCURACY_VALUE',
'Maximum model space distance between geometric entities at asserted c
onnectivities');
#24979=UNCERTAINTY_MEASURE_WITH_UNIT(LENGTH_MEASURE(0.001),#25101,
'DISTANCE_ACCURACY_VALUE',
'Maximum model space distance between geometric entities at asserted c
onnectivities');
#25067=(
GEOMETRIC_REPRESENTATION_CONTEXT(3)
GLOBAL_UNCERTAINTY_ASSIGNED_CONTEXT((#24946))
GLOBAL_UNIT_ASSIGNED_CONTEXT((#25101,#25103,#25104))
REPRESENTATION_CONTEXT('','3D')
);
#25100=(
GEOMETRIC_REPRESENTATION_CONTEXT(3)
GLOBAL_UNCERTAINTY_ASSIGNED_CONTEXT((#24979))
GLOBAL_UNIT_ASSIGNED_CONTEXT((#25101,#25103,#25104))
REPRESENTATION_CONTEXT('','3D')
);
#25101=(
LENGTH_UNIT()
NAMED_UNIT(*)
SI_UNIT(.CENTI.,.METRE.)
);
#25103=(
NAMED_UNIT(*)
PLANE_ANGLE_UNIT()
SI_UNIT($,.RADIAN.)
);
#25104=(
NAMED_UNIT(*)
SI_UNIT($,.STERADIAN.)
SOLID_ANGLE_UNIT()
);
#25192=SHAPE_DEFINITION_REPRESENTATION(#25386,#25597);
#25386=PRODUCT_DEFINITION_SHAPE('',$,#25718);
#25597=SHAPE_REPRESENTATION('',(#15871),#25067);
#25630=PRODUCT_DEFINITION_CONTEXT('part definition',#25992,'design');
#25718=PRODUCT_DEFINITION('M4 low-profile retaining screw (2)',
'M4 low-profile retaining screw (2)',#25838,#25630);
#25838=PRODUCT_DEFINITION_FORMATION('',$,#26081);
#25992=APPLICATION_CONTEXT(
'Core Data for Automotive Mechanical Design Process');
#25993=PRODUCT_CONTEXT('part definition',#25992,'mechanical');
#26081=PRODUCT('M4 low-profile retaining screw (2)',
'M4 low-profile retaining screw (2)','M4 low-profile retaining screw (2)',(#25993));
#26192=COLOUR_RGB('Black',0.12,0.14,0.17);
#26193=FILL_AREA_STYLE_COLOUR('',#26192);
#26194=FILL_AREA_STYLE('',(#26193));
#26195=SURFACE_STYLE_FILL_AREA(#26194);
#26196=SURFACE_SIDE_STYLE('',(#26195));
#26197=SURFACE_STYLE_USAGE(.BOTH.,#26196);
#26198=PRESENTATION_STYLE_ASSIGNMENT((#26197));
ENDSEC;
END-ISO-10303-21;
